ISO-10303-21;
HEADER;
/* Generated by software containing ST-Developer
 * from STEP Tools, Inc. (www.steptools.com) 
 */

FILE_DESCRIPTION(
/* description */ ('Independently dimensioned six-bar single-leg walking-linkage demonstr
ator. Whole-mm20 crank,60 upper rocker,80/120 ternary coupler,120 lowe
r rocker,140 knee pitch and260 toe reach; ground pivots0/0,60/0,40/60.
 Seven native revolutes close both loops. Four reused native library f
amilies, fully retained shared pins and layered real spacer stacks, bo
nded rubber toe. Benchtop reference mechanism; no complete vehicle, lo
ad, gait stability, adhesive, weld, fit or life rating.'),
/* implementation_level */ '2;1');

FILE_NAME(
/* name */ 'Pivot washer.step',
/* time_stamp */ '2026-11-09T20:33:14-08:00',
/* author */ (''),
/* organization */ (''),
/* preprocessor_version */ 'ST-DEVELOPER v20.2',
/* originating_system */ 'Autodesk Translation Framework v15.17.0.0',
/* authorisation */ '');

FILE_SCHEMA (('AUTOMOTIVE_DESIGN { 1 0 10303 214 3 1 1 }'));
ENDSEC;

DATA;
#10=MECHANICAL_DESIGN_GEOMETRIC_PRESENTATION_REPRESENTATION('',(#266),#4048);
#230=SHAPE_REPRESENTATION_RELATIONSHIP('SRR','None',#4154,#248);
#248=ADVANCED_BREP_SHAPE_REPRESENTATION('',(#284),#4041);
#266=STYLED_ITEM('',(#4252),#284);
#284=MANIFOLD_SOLID_BREP('Body1',#2155);
#334=FACE_BOUND('',#673,.T.);
#335=FACE_BOUND('',#675,.T.);
#393=PLANE('',#2544);
#394=PLANE('',#2545);
#501=FACE_OUTER_BOUND('',#670,.T.);
#502=FACE_OUTER_BOUND('',#671,.T.);
#503=FACE_OUTER_BOUND('',#672,.T.);
#504=FACE_OUTER_BOUND('',#674,.T.);
#670=EDGE_LOOP('',(#1843,#1844,#1845,#1846));
#671=EDGE_LOOP('',(#1847,#1848,#1849,#1850));
#672=EDGE_LOOP('',(#1851));
#673=EDGE_LOOP('',(#1852));
#674=EDGE_LOOP('',(#1853));
#675=EDGE_LOOP('',(#1854));
#825=LINE('',#3816,#950);
#826=LINE('',#3822,#951);
#950=VECTOR('',#3130,5.);
#951=VECTOR('',#3137,10.);
#1052=CIRCLE('',#2539,5.);
#1053=CIRCLE('',#2540,5.);
#1054=CIRCLE('',#2542,10.);
#1055=CIRCLE('',#2543,10.);
#1206=VERTEX_POINT('',#3813);
#1207=VERTEX_POINT('',#3815);
#1208=VERTEX_POINT('',#3819);
#1209=VERTEX_POINT('',#3821);
#1425=EDGE_CURVE('',#1206,#1206,#1052,.T.);
#1426=EDGE_CURVE('',#1206,#1207,#825,.T.);
#1427=EDGE_CURVE('',#1207,#1207,#1053,.T.);
#1428=EDGE_CURVE('',#1208,#1208,#1054,.T.);
#1429=EDGE_CURVE('',#1208,#1209,#826,.T.);
#1430=EDGE_CURVE('',#1209,#1209,#1055,.T.);
#1843=ORIENTED_EDGE('',*,*,#1425,.F.);
#1844=ORIENTED_EDGE('',*,*,#1426,.T.);
#1845=ORIENTED_EDGE('',*,*,#1427,.T.);
#1846=ORIENTED_EDGE('',*,*,#1426,.F.);
#1847=ORIENTED_EDGE('',*,*,#1428,.F.);
#1848=ORIENTED_EDGE('',*,*,#1429,.T.);
#1849=ORIENTED_EDGE('',*,*,#1430,.T.);
#1850=ORIENTED_EDGE('',*,*,#1429,.F.);
#1851=ORIENTED_EDGE('',*,*,#1428,.T.);
#1852=ORIENTED_EDGE('',*,*,#1425,.T.);
#1853=ORIENTED_EDGE('',*,*,#1430,.F.);
#1854=ORIENTED_EDGE('',*,*,#1427,.F.);
#2000=CYLINDRICAL_SURFACE('',#2538,5.);
#2001=CYLINDRICAL_SURFACE('',#2541,10.);
#2104=ADVANCED_FACE('',(#501),#2000,.F.);
#2105=ADVANCED_FACE('',(#502),#2001,.T.);
#2106=ADVANCED_FACE('',(#503,#334),#393,.T.);
#2107=ADVANCED_FACE('',(#504,#335),#394,.F.);
#2155=CLOSED_SHELL('',(#2104,#2105,#2106,#2107));
#2537=AXIS2_PLACEMENT_3D('',#3811,#3124,#3125);
#2538=AXIS2_PLACEMENT_3D('',#3812,#3126,#3127);
#2539=AXIS2_PLACEMENT_3D('',#3814,#3128,#3129);
#2540=AXIS2_PLACEMENT_3D('',#3817,#3131,#3132);
#2541=AXIS2_PLACEMENT_3D('',#3818,#3133,#3134);
#2542=AXIS2_PLACEMENT_3D('',#3820,#3135,#3136);
#2543=AXIS2_PLACEMENT_3D('',#3823,#3138,#3139);
#2544=AXIS2_PLACEMENT_3D('',#3824,#3140,#3141);
#2545=AXIS2_PLACEMENT_3D('',#3825,#3142,#3143);
#3124=DIRECTION('axis',(0.,0.,1.));
#3125=DIRECTION('refdir',(1.,0.,0.));
#3126=DIRECTION('center_axis',(0.,0.,1.));
#3127=DIRECTION('ref_axis',(1.,0.,0.));
#3128=DIRECTION('center_axis',(0.,0.,-1.));
#3129=DIRECTION('ref_axis',(1.,0.,0.));
#3130=DIRECTION('',(0.,0.,-1.));
#3131=DIRECTION('center_axis',(0.,0.,-1.));
#3132=DIRECTION('ref_axis',(1.,0.,0.));
#3133=DIRECTION('center_axis',(0.,0.,1.));
#3134=DIRECTION('ref_axis',(1.,0.,0.));
#3135=DIRECTION('center_axis',(0.,0.,1.));
#3136=DIRECTION('ref_axis',(1.,0.,0.));
#3137=DIRECTION('',(0.,0.,-1.));
#3138=DIRECTION('center_axis',(0.,0.,1.));
#3139=DIRECTION('ref_axis',(1.,0.,0.));
#3140=DIRECTION('center_axis',(0.,0.,1.));
#3141=DIRECTION('ref_axis',(1.,0.,0.));
#3142=DIRECTION('center_axis',(0.,0.,1.));
#3143=DIRECTION('ref_axis',(1.,0.,0.));
#3811=CARTESIAN_POINT('',(0.,0.,0.));
#3812=CARTESIAN_POINT('Origin',(0.,0.,0.));
#3813=CARTESIAN_POINT('',(-5.,-6.12323399573677E-16,2.));
#3814=CARTESIAN_POINT('Origin',(0.,0.,2.));
#3815=CARTESIAN_POINT('',(-5.,-6.12323399573677E-16,0.));
#3816=CARTESIAN_POINT('',(-5.,-6.12323399573677E-16,0.));
#3817=CARTESIAN_POINT('Origin',(0.,0.,0.));
#3818=CARTESIAN_POINT('Origin',(0.,0.,0.));
#3819=CARTESIAN_POINT('',(-10.,-1.22464679914735E-15,2.));
#3820=CARTESIAN_POINT('Origin',(0.,0.,2.));
#3821=CARTESIAN_POINT('',(-10.,-1.22464679914735E-15,0.));
#3822=CARTESIAN_POINT('',(-10.,-1.22464679914735E-15,0.));
#3823=CARTESIAN_POINT('Origin',(0.,0.,0.));
#3824=CARTESIAN_POINT('Origin',(0.,0.,2.));
#3825=CARTESIAN_POINT('Origin',(0.,0.,0.));
#4021=UNCERTAINTY_MEASURE_WITH_UNIT(LENGTH_MEASURE(0.01),#4049,
'DISTANCE_ACCURACY_VALUE',
'Maximum model space distance between geometric entities at asserted c
onnectivities');
#4028=UNCERTAINTY_MEASURE_WITH_UNIT(LENGTH_MEASURE(0.01),#4049,
'DISTANCE_ACCURACY_VALUE',
'Maximum model space distance between geometric entities at asserted c
onnectivities');
#4041=(
GEOMETRIC_REPRESENTATION_CONTEXT(3)
GLOBAL_UNCERTAINTY_ASSIGNED_CONTEXT((#4021))
GLOBAL_UNIT_ASSIGNED_CONTEXT((#4049,#4051,#4052))
REPRESENTATION_CONTEXT('','3D')
);
#4048=(
GEOMETRIC_REPRESENTATION_CONTEXT(3)
GLOBAL_UNCERTAINTY_ASSIGNED_CONTEXT((#4028))
GLOBAL_UNIT_ASSIGNED_CONTEXT((#4049,#4051,#4052))
REPRESENTATION_CONTEXT('','3D')
);
#4049=(
LENGTH_UNIT()
NAMED_UNIT(*)
SI_UNIT(.MILLI.,.METRE.)
);
#4051=(
NAMED_UNIT(*)
PLANE_ANGLE_UNIT()
SI_UNIT($,.RADIAN.)
);
#4052=(
NAMED_UNIT(*)
SI_UNIT($,.STERADIAN.)
SOLID_ANGLE_UNIT()
);
#4065=SHAPE_DEFINITION_REPRESENTATION(#4084,#4154);
#4084=PRODUCT_DEFINITION_SHAPE('',$,#4174);
#4154=SHAPE_REPRESENTATION('',(#2537),#4041);
#4161=PRODUCT_DEFINITION_CONTEXT('part definition',#4220,'design');
#4174=PRODUCT_DEFINITION('Pivot washer','Pivot washer',#4193,#4161);
#4193=PRODUCT_DEFINITION_FORMATION('',$,#4234);
#4220=APPLICATION_CONTEXT(
'Core Data for Automotive Mechanical Design Process');
#4221=PRODUCT_CONTEXT('part definition',#4220,'mechanical');
#4234=PRODUCT('Pivot washer','Pivot washer',$,(#4221));
#4252=PRESENTATION_STYLE_ASSIGNMENT((#4266));
#4266=SURFACE_STYLE_USAGE(.BOTH.,#4280);
#4280=SURFACE_SIDE_STYLE('',(#4294));
#4294=SURFACE_STYLE_FILL_AREA(#4308);
#4308=FILL_AREA_STYLE('Washer light gray',(#4322));
#4322=FILL_AREA_STYLE_COLOUR('Washer light gray',#4336);
#4336=COLOUR_RGB('Washer light gray',0.725490196078431,0.752941176470588,
0.792156862745098);
ENDSEC;
END-ISO-10303-21;
